ISO-10303-21;
HEADER;
/* Generated by software containing ST-Developer
 * from STEP Tools, Inc. (www.steptools.com) 
 */

FILE_DESCRIPTION(
/* description */ ('Bin tilter linkage'),
/* implementation_level */ '2;1');

FILE_NAME(
/* name */ 'M4 short cap screw (3).step',
/* time_stamp */ '2026-10-28T03:26:24-07:00',
/* author */ (''),
/* organization */ (''),
/* preprocessor_version */ 'ST-DEVELOPER v20.2',
/* originating_system */ 'Autodesk Translation Framework v15.17.0.0',
/* authorisation */ '');

FILE_SCHEMA (('AUTOMOTIVE_DESIGN { 1 0 10303 214 3 1 1 }'));
ENDSEC;

DATA;
#10=MECHANICAL_DESIGN_GEOMETRIC_PRESENTATION_REPRESENTATION('',(#897),#23728);
#685=SHAPE_REPRESENTATION_RELATIONSHIP('SRR','None',#24150,#791);
#791=ADVANCED_BREP_SHAPE_REPRESENTATION('',(#1010),#23650);
#897=STYLED_ITEM('',(#24772),#1010);
#1010=MANIFOLD_SOLID_BREP('Body1',#12428);
#1267=FACE_BOUND('',#3136,.T.);
#1632=PLANE('',#14295);
#1633=PLANE('',#14300);
#1634=PLANE('',#14303);
#2178=FACE_OUTER_BOUND('',#3135,.T.);
#2179=FACE_OUTER_BOUND('',#3137,.T.);
#2180=FACE_OUTER_BOUND('',#3138,.T.);
#2181=FACE_OUTER_BOUND('',#3139,.T.);
#2182=FACE_OUTER_BOUND('',#3140,.T.);
#3135=EDGE_LOOP('',(#9529));
#3136=EDGE_LOOP('',(#9530));
#3137=EDGE_LOOP('',(#9531,#9532,#9533,#9534));
#3138=EDGE_LOOP('',(#9535));
#3139=EDGE_LOOP('',(#9536,#9537,#9538,#9539));
#3140=EDGE_LOOP('',(#9540));
#4135=LINE('',#21041,#4810);
#4136=LINE('',#21047,#4811);
#4810=VECTOR('',#17006,0.35);
#4811=VECTOR('',#17015,0.2);
#5491=CIRCLE('',#14296,0.35);
#5492=CIRCLE('',#14297,0.2);
#5493=CIRCLE('',#14299,0.35);
#5494=CIRCLE('',#14302,0.2);
#6341=VERTEX_POINT('',#21035);
#6342=VERTEX_POINT('',#21037);
#6343=VERTEX_POINT('',#21040);
#6344=VERTEX_POINT('',#21045);
#7504=EDGE_CURVE('',#6341,#6341,#5491,.T.);
#7505=EDGE_CURVE('',#6342,#6342,#5492,.T.);
#7506=EDGE_CURVE('',#6341,#6343,#4135,.T.);
#7507=EDGE_CURVE('',#6343,#6343,#5493,.T.);
#7508=EDGE_CURVE('',#6344,#6344,#5494,.T.);
#7509=EDGE_CURVE('',#6344,#6342,#4136,.T.);
#9529=ORIENTED_EDGE('',*,*,#7504,.T.);
#9530=ORIENTED_EDGE('',*,*,#7505,.F.);
#9531=ORIENTED_EDGE('',*,*,#7504,.F.);
#9532=ORIENTED_EDGE('',*,*,#7506,.T.);
#9533=ORIENTED_EDGE('',*,*,#7507,.T.);
#9534=ORIENTED_EDGE('',*,*,#7506,.F.);
#9535=ORIENTED_EDGE('',*,*,#7507,.F.);
#9536=ORIENTED_EDGE('',*,*,#7508,.F.);
#9537=ORIENTED_EDGE('',*,*,#7509,.T.);
#9538=ORIENTED_EDGE('',*,*,#7505,.T.);
#9539=ORIENTED_EDGE('',*,*,#7509,.F.);
#9540=ORIENTED_EDGE('',*,*,#7508,.T.);
#11411=CYLINDRICAL_SURFACE('',#14298,0.35);
#11412=CYLINDRICAL_SURFACE('',#14301,0.2);
#11903=ADVANCED_FACE('',(#2178,#1267),#1632,.T.);
#11904=ADVANCED_FACE('',(#2179),#11411,.T.);
#11905=ADVANCED_FACE('',(#2180),#1633,.F.);
#11906=ADVANCED_FACE('',(#2181),#11412,.T.);
#11907=ADVANCED_FACE('',(#2182),#1634,.T.);
#12428=CLOSED_SHELL('',(#11903,#11904,#11905,#11906,#11907));
#14294=AXIS2_PLACEMENT_3D('',#21033,#16996,#16997);
#14295=AXIS2_PLACEMENT_3D('',#21034,#16998,#16999);
#14296=AXIS2_PLACEMENT_3D('',#21036,#17000,#17001);
#14297=AXIS2_PLACEMENT_3D('',#21038,#17002,#17003);
#14298=AXIS2_PLACEMENT_3D('',#21039,#17004,#17005);
#14299=AXIS2_PLACEMENT_3D('',#21042,#17007,#17008);
#14300=AXIS2_PLACEMENT_3D('',#21043,#17009,#17010);
#14301=AXIS2_PLACEMENT_3D('',#21044,#17011,#17012);
#14302=AXIS2_PLACEMENT_3D('',#21046,#17013,#17014);
#14303=AXIS2_PLACEMENT_3D('',#21048,#17016,#17017);
#16996=DIRECTION('axis',(0.,0.,1.));
#16997=DIRECTION('refdir',(1.,0.,0.));
#16998=DIRECTION('center_axis',(0.,1.,0.));
#16999=DIRECTION('ref_axis',(1.,0.,0.));
#17000=DIRECTION('center_axis',(0.,1.,0.));
#17001=DIRECTION('ref_axis',(1.,0.,0.));
#17002=DIRECTION('center_axis',(0.,1.,0.));
#17003=DIRECTION('ref_axis',(1.,0.,0.));
#17004=DIRECTION('center_axis',(0.,1.,0.));
#17005=DIRECTION('ref_axis',(1.,0.,0.));
#17006=DIRECTION('',(0.,-1.,0.));
#17007=DIRECTION('center_axis',(0.,1.,0.));
#17008=DIRECTION('ref_axis',(1.,0.,0.));
#17009=DIRECTION('center_axis',(0.,1.,0.));
#17010=DIRECTION('ref_axis',(1.,0.,0.));
#17011=DIRECTION('center_axis',(0.,1.,0.));
#17012=DIRECTION('ref_axis',(1.,0.,0.));
#17013=DIRECTION('center_axis',(0.,1.,0.));
#17014=DIRECTION('ref_axis',(1.,0.,0.));
#17015=DIRECTION('',(0.,-1.,0.));
#17016=DIRECTION('center_axis',(0.,1.,0.));
#17017=DIRECTION('ref_axis',(1.,0.,0.));
#21033=CARTESIAN_POINT('',(0.,0.,0.));
#21034=CARTESIAN_POINT('Origin',(1.30814754519511,-0.8,13.6918524548049));
#21035=CARTESIAN_POINT('',(0.958147545195112,-0.8,13.6918524548049));
#21036=CARTESIAN_POINT('Origin',(1.30814754519511,-0.8,13.6918524548049));
#21037=CARTESIAN_POINT('',(1.10814754519511,-0.8,13.6918524548049));
#21038=CARTESIAN_POINT('Origin',(1.30814754519511,-0.8,13.6918524548049));
#21039=CARTESIAN_POINT('Origin',(1.30814754519511,-1.2,13.6918524548049));
#21040=CARTESIAN_POINT('',(0.958147545195112,-1.2,13.6918524548049));
#21041=CARTESIAN_POINT('',(0.958147545195112,-1.2,13.6918524548049));
#21042=CARTESIAN_POINT('Origin',(1.30814754519511,-1.2,13.6918524548049));
#21043=CARTESIAN_POINT('Origin',(1.30814754519511,-1.2,13.6918524548049));
#21044=CARTESIAN_POINT('Origin',(1.30814754519511,-0.8,13.6918524548049));
#21045=CARTESIAN_POINT('',(1.10814754519511,-0.1,13.6918524548049));
#21046=CARTESIAN_POINT('Origin',(1.30814754519511,-0.1,13.6918524548049));
#21047=CARTESIAN_POINT('',(1.10814754519511,-0.8,13.6918524548049));
#21048=CARTESIAN_POINT('Origin',(1.30814754519511,-0.1,13.6918524548049));
#23533=UNCERTAINTY_MEASURE_WITH_UNIT(LENGTH_MEASURE(0.001),#23729,
'DISTANCE_ACCURACY_VALUE',
'Maximum model space distance between geometric entities at asserted c
onnectivities');
#23611=UNCERTAINTY_MEASURE_WITH_UNIT(LENGTH_MEASURE(0.001),#23729,
'DISTANCE_ACCURACY_VALUE',
'Maximum model space distance between geometric entities at asserted c
onnectivities');
#23650=(
GEOMETRIC_REPRESENTATION_CONTEXT(3)
GLOBAL_UNCERTAINTY_ASSIGNED_CONTEXT((#23533))
GLOBAL_UNIT_ASSIGNED_CONTEXT((#23729,#23731,#23732))
REPRESENTATION_CONTEXT('','3D')
);
#23728=(
GEOMETRIC_REPRESENTATION_CONTEXT(3)
GLOBAL_UNCERTAINTY_ASSIGNED_CONTEXT((#23611))
GLOBAL_UNIT_ASSIGNED_CONTEXT((#23729,#23731,#23732))
REPRESENTATION_CONTEXT('','3D')
);
#23729=(
LENGTH_UNIT()
NAMED_UNIT(*)
SI_UNIT(.CENTI.,.METRE.)
);
#23731=(
NAMED_UNIT(*)
PLANE_ANGLE_UNIT()
SI_UNIT($,.RADIAN.)
);
#23732=(
NAMED_UNIT(*)
SI_UNIT($,.STERADIAN.)
SOLID_ANGLE_UNIT()
);
#23771=SHAPE_DEFINITION_REPRESENTATION(#23887,#24150);
#23887=PRODUCT_DEFINITION_SHAPE('',$,#24267);
#24150=SHAPE_REPRESENTATION('',(#14294),#23650);
#24228=PRODUCT_DEFINITION_CONTEXT('part definition',#24578,'design');
#24267=PRODUCT_DEFINITION('M4 short cap screw (3)',
'M4 short cap screw (3)',#24383,#24228);
#24383=PRODUCT_DEFINITION_FORMATION('',$,#24618);
#24578=APPLICATION_CONTEXT(
'Core Data for Automotive Mechanical Design Process');
#24579=PRODUCT_CONTEXT('part definition',#24578,'mechanical');
#24618=PRODUCT('M4 short cap screw (3)','M4 short cap screw (3)',
'M4 short cap screw (3)',(#24579));
#24766=COLOUR_RGB('Black',0.12,0.14,0.17);
#24767=FILL_AREA_STYLE_COLOUR('',#24766);
#24768=FILL_AREA_STYLE('',(#24767));
#24769=SURFACE_STYLE_FILL_AREA(#24768);
#24770=SURFACE_SIDE_STYLE('',(#24769));
#24771=SURFACE_STYLE_USAGE(.BOTH.,#24770);
#24772=PRESENTATION_STYLE_ASSIGNMENT((#24771));
ENDSEC;
END-ISO-10303-21;
